ISO-10303-21;
HEADER;
/* Generated by software containing ST-Developer
 * from STEP Tools, Inc. (www.steptools.com) 
 */

FILE_DESCRIPTION(
/* description */ ('STEP AP203'),
/* implementation_level */ '2;1');

FILE_NAME(
/* name */ 'F04_M5_Gib_Adjusting_Screw.step',
/* time_stamp */ '2026-11-15T15:04:01-08:00',
/* author */ (''),
/* organization */ (''),
/* preprocessor_version */ 'ST-DEVELOPER v20.2',
/* originating_system */ 'Autodesk Translation Framework v15.17.0.0',
/* authorisation */ '');

FILE_SCHEMA (('AUTOMOTIVE_DESIGN { 1 0 10303 214 3 1 1 }'));
ENDSEC;

DATA;
#10=MECHANICAL_DESIGN_GEOMETRIC_PRESENTATION_REPRESENTATION('',(#304),#16598);
#226=SHAPE_REPRESENTATION_RELATIONSHIP('SRR','None',#16720,#250);
#250=ADVANCED_BREP_SHAPE_REPRESENTATION('',(#274),#16596);
#274=MANIFOLD_SOLID_BREP('Body1',#9809);
#304=STYLED_ITEM('',(#16832),#274);
#426=FACE_BOUND('',#2119,.T.);
#892=PLANE('',#10858);
#893=PLANE('',#10859);
#894=PLANE('',#10860);
#895=PLANE('',#10861);
#896=PLANE('',#10862);
#897=PLANE('',#10863);
#898=PLANE('',#10864);
#899=PLANE('',#10865);
#900=PLANE('',#10866);
#1440=FACE_OUTER_BOUND('',#2111,.T.);
#1441=FACE_OUTER_BOUND('',#2112,.T.);
#1442=FACE_OUTER_BOUND('',#2113,.T.);
#1443=FACE_OUTER_BOUND('',#2114,.T.);
#1444=FACE_OUTER_BOUND('',#2115,.T.);
#1445=FACE_OUTER_BOUND('',#2116,.T.);
#1446=FACE_OUTER_BOUND('',#2117,.T.);
#1447=FACE_OUTER_BOUND('',#2118,.T.);
#1448=FACE_OUTER_BOUND('',#2120,.T.);
#1449=FACE_OUTER_BOUND('',#2121,.T.);
#2111=EDGE_LOOP('',(#9079,#9080,#9081,#9082));
#2112=EDGE_LOOP('',(#9083,#9084,#9085,#9086));
#2113=EDGE_LOOP('',(#9087,#9088,#9089,#9090));
#2114=EDGE_LOOP('',(#9091,#9092,#9093,#9094));
#2115=EDGE_LOOP('',(#9095,#9096,#9097,#9098));
#2116=EDGE_LOOP('',(#9099,#9100,#9101,#9102));
#2117=EDGE_LOOP('',(#9103,#9104,#9105,#9106));
#2118=EDGE_LOOP('',(#9107,#9108,#9109,#9110,#9111,#9112));
#2119=EDGE_LOOP('',(#9113));
#2120=EDGE_LOOP('',(#9114,#9115,#9116,#9117,#9118,#9119));
#2121=EDGE_LOOP('',(#9120));
#3145=LINE('',#16409,#4193);
#3146=LINE('',#16414,#4194);
#3147=LINE('',#16416,#4195);
#3148=LINE('',#16418,#4196);
#3149=LINE('',#16419,#4197);
#3150=LINE('',#16422,#4198);
#3151=LINE('',#16424,#4199);
#3152=LINE('',#16425,#4200);
#3153=LINE('',#16428,#4201);
#3154=LINE('',#16430,#4202);
#3155=LINE('',#16431,#4203);
#3156=LINE('',#16434,#4204);
#3157=LINE('',#16436,#4205);
#3158=LINE('',#16437,#4206);
#3159=LINE('',#16440,#4207);
#3160=LINE('',#16442,#4208);
#3161=LINE('',#16443,#4209);
#3162=LINE('',#16445,#4210);
#3163=LINE('',#16446,#4211);
#4193=VECTOR('',#13499,2.);
#4194=VECTOR('',#13504,1000.);
#4195=VECTOR('',#13505,1000.);
#4196=VECTOR('',#13506,1000.);
#4197=VECTOR('',#13507,1000.);
#4198=VECTOR('',#13510,1000.);
#4199=VECTOR('',#13511,1000.);
#4200=VECTOR('',#13512,1000.);
#4201=VECTOR('',#13515,1000.);
#4202=VECTOR('',#13516,1000.);
#4203=VECTOR('',#13517,1000.);
#4204=VECTOR('',#13520,1000.);
#4205=VECTOR('',#13521,1000.);
#4206=VECTOR('',#13522,1000.);
#4207=VECTOR('',#13525,1000.);
#4208=VECTOR('',#13526,1000.);
#4209=VECTOR('',#13527,1000.);
#4210=VECTOR('',#13530,1000.);
#4211=VECTOR('',#13531,1000.);
#4449=CIRCLE('',#10856,2.);
#4450=CIRCLE('',#10857,2.);
#5281=VERTEX_POINT('',#16406);
#5282=VERTEX_POINT('',#16408);
#5283=VERTEX_POINT('',#16412);
#5284=VERTEX_POINT('',#16413);
#5285=VERTEX_POINT('',#16415);
#5286=VERTEX_POINT('',#16417);
#5287=VERTEX_POINT('',#16421);
#5288=VERTEX_POINT('',#16423);
#5289=VERTEX_POINT('',#16427);
#5290=VERTEX_POINT('',#16429);
#5291=VERTEX_POINT('',#16433);
#5292=VERTEX_POINT('',#16435);
#5293=VERTEX_POINT('',#16439);
#5294=VERTEX_POINT('',#16441);
#6552=EDGE_CURVE('',#5281,#5281,#4449,.T.);
#6553=EDGE_CURVE('',#5281,#5282,#3145,.T.);
#6554=EDGE_CURVE('',#5282,#5282,#4450,.T.);
#6555=EDGE_CURVE('',#5283,#5284,#3146,.T.);
#6556=EDGE_CURVE('',#5285,#5284,#3147,.T.);
#6557=EDGE_CURVE('',#5286,#5285,#3148,.T.);
#6558=EDGE_CURVE('',#5286,#5283,#3149,.T.);
#6559=EDGE_CURVE('',#5284,#5287,#3150,.T.);
#6560=EDGE_CURVE('',#5288,#5287,#3151,.T.);
#6561=EDGE_CURVE('',#5285,#5288,#3152,.T.);
#6562=EDGE_CURVE('',#5287,#5289,#3153,.T.);
#6563=EDGE_CURVE('',#5290,#5289,#3154,.T.);
#6564=EDGE_CURVE('',#5288,#5290,#3155,.T.);
#6565=EDGE_CURVE('',#5289,#5291,#3156,.T.);
#6566=EDGE_CURVE('',#5292,#5291,#3157,.T.);
#6567=EDGE_CURVE('',#5290,#5292,#3158,.T.);
#6568=EDGE_CURVE('',#5291,#5293,#3159,.T.);
#6569=EDGE_CURVE('',#5294,#5293,#3160,.T.);
#6570=EDGE_CURVE('',#5292,#5294,#3161,.T.);
#6571=EDGE_CURVE('',#5293,#5283,#3162,.T.);
#6572=EDGE_CURVE('',#5294,#5286,#3163,.T.);
#9079=ORIENTED_EDGE('',*,*,#6552,.T.);
#9080=ORIENTED_EDGE('',*,*,#6553,.T.);
#9081=ORIENTED_EDGE('',*,*,#6554,.F.);
#9082=ORIENTED_EDGE('',*,*,#6553,.F.);
#9083=ORIENTED_EDGE('',*,*,#6555,.T.);
#9084=ORIENTED_EDGE('',*,*,#6556,.F.);
#9085=ORIENTED_EDGE('',*,*,#6557,.F.);
#9086=ORIENTED_EDGE('',*,*,#6558,.T.);
#9087=ORIENTED_EDGE('',*,*,#6559,.T.);
#9088=ORIENTED_EDGE('',*,*,#6560,.F.);
#9089=ORIENTED_EDGE('',*,*,#6561,.F.);
#9090=ORIENTED_EDGE('',*,*,#6556,.T.);
#9091=ORIENTED_EDGE('',*,*,#6562,.T.);
#9092=ORIENTED_EDGE('',*,*,#6563,.F.);
#9093=ORIENTED_EDGE('',*,*,#6564,.F.);
#9094=ORIENTED_EDGE('',*,*,#6560,.T.);
#9095=ORIENTED_EDGE('',*,*,#6565,.T.);
#9096=ORIENTED_EDGE('',*,*,#6566,.F.);
#9097=ORIENTED_EDGE('',*,*,#6567,.F.);
#9098=ORIENTED_EDGE('',*,*,#6563,.T.);
#9099=ORIENTED_EDGE('',*,*,#6568,.T.);
#9100=ORIENTED_EDGE('',*,*,#6569,.F.);
#9101=ORIENTED_EDGE('',*,*,#6570,.F.);
#9102=ORIENTED_EDGE('',*,*,#6566,.T.);
#9103=ORIENTED_EDGE('',*,*,#6571,.T.);
#9104=ORIENTED_EDGE('',*,*,#6558,.F.);
#9105=ORIENTED_EDGE('',*,*,#6572,.F.);
#9106=ORIENTED_EDGE('',*,*,#6569,.T.);
#9107=ORIENTED_EDGE('',*,*,#6557,.T.);
#9108=ORIENTED_EDGE('',*,*,#6561,.T.);
#9109=ORIENTED_EDGE('',*,*,#6564,.T.);
#9110=ORIENTED_EDGE('',*,*,#6567,.T.);
#9111=ORIENTED_EDGE('',*,*,#6570,.T.);
#9112=ORIENTED_EDGE('',*,*,#6572,.T.);
#9113=ORIENTED_EDGE('',*,*,#6552,.F.);
#9114=ORIENTED_EDGE('',*,*,#6555,.F.);
#9115=ORIENTED_EDGE('',*,*,#6571,.F.);
#9116=ORIENTED_EDGE('',*,*,#6568,.F.);
#9117=ORIENTED_EDGE('',*,*,#6565,.F.);
#9118=ORIENTED_EDGE('',*,*,#6562,.F.);
#9119=ORIENTED_EDGE('',*,*,#6559,.F.);
#9120=ORIENTED_EDGE('',*,*,#6554,.T.);
#9233=CYLINDRICAL_SURFACE('',#10855,2.);
#9765=ADVANCED_FACE('',(#1440),#9233,.T.);
#9766=ADVANCED_FACE('',(#1441),#892,.F.);
#9767=ADVANCED_FACE('',(#1442),#893,.F.);
#9768=ADVANCED_FACE('',(#1443),#894,.F.);
#9769=ADVANCED_FACE('',(#1444),#895,.F.);
#9770=ADVANCED_FACE('',(#1445),#896,.F.);
#9771=ADVANCED_FACE('',(#1446),#897,.F.);
#9772=ADVANCED_FACE('',(#1447,#426),#898,.T.);
#9773=ADVANCED_FACE('',(#1448),#899,.F.);
#9774=ADVANCED_FACE('',(#1449),#900,.T.);
#9809=CLOSED_SHELL('',(#9765,#9766,#9767,#9768,#9769,#9770,#9771,#9772,
#9773,#9774));
#10854=AXIS2_PLACEMENT_3D('',#16404,#13493,#13494);
#10855=AXIS2_PLACEMENT_3D('',#16405,#13495,#13496);
#10856=AXIS2_PLACEMENT_3D('',#16407,#13497,#13498);
#10857=AXIS2_PLACEMENT_3D('',#16410,#13500,#13501);
#10858=AXIS2_PLACEMENT_3D('',#16411,#13502,#13503);
#10859=AXIS2_PLACEMENT_3D('',#16420,#13508,#13509);
#10860=AXIS2_PLACEMENT_3D('',#16426,#13513,#13514);
#10861=AXIS2_PLACEMENT_3D('',#16432,#13518,#13519);
#10862=AXIS2_PLACEMENT_3D('',#16438,#13523,#13524);
#10863=AXIS2_PLACEMENT_3D('',#16444,#13528,#13529);
#10864=AXIS2_PLACEMENT_3D('',#16447,#13532,#13533);
#10865=AXIS2_PLACEMENT_3D('',#16448,#13534,#13535);
#10866=AXIS2_PLACEMENT_3D('',#16449,#13536,#13537);
#13493=DIRECTION('axis',(0.,0.,1.));
#13494=DIRECTION('refdir',(1.,0.,0.));
#13495=DIRECTION('center_axis',(0.,0.,-1.));
#13496=DIRECTION('ref_axis',(-1.,0.,0.));
#13497=DIRECTION('center_axis',(0.,0.,1.));
#13498=DIRECTION('ref_axis',(1.,0.,0.));
#13499=DIRECTION('',(0.,0.,1.));
#13500=DIRECTION('center_axis',(0.,0.,1.));
#13501=DIRECTION('ref_axis',(1.,0.,0.));
#13502=DIRECTION('center_axis',(-0.866025403784439,0.5,0.));
#13503=DIRECTION('ref_axis',(-0.5,-0.866025403784439,0.));
#13504=DIRECTION('',(0.5,0.866025403784439,0.));
#13505=DIRECTION('',(0.,0.,-1.));
#13506=DIRECTION('',(0.5,0.866025403784439,0.));
#13507=DIRECTION('',(0.,0.,-1.));
#13508=DIRECTION('center_axis',(-0.866025403784439,-0.5,0.));
#13509=DIRECTION('ref_axis',(0.5,-0.866025403784439,0.));
#13510=DIRECTION('',(-0.5,0.866025403784439,0.));
#13511=DIRECTION('',(0.,0.,-1.));
#13512=DIRECTION('',(-0.5,0.866025403784439,0.));
#13513=DIRECTION('center_axis',(-1.87789324842145E-16,-1.,0.));
#13514=DIRECTION('ref_axis',(1.,-1.87789324842145E-16,0.));
#13515=DIRECTION('',(-1.,1.87789324842145E-16,0.));
#13516=DIRECTION('',(0.,0.,-1.));
#13517=DIRECTION('',(-1.,1.87789324842145E-16,0.));
#13518=DIRECTION('center_axis',(0.866025403784438,-0.5,0.));
#13519=DIRECTION('ref_axis',(0.5,0.866025403784438,0.));
#13520=DIRECTION('',(-0.5,-0.866025403784438,0.));
#13521=DIRECTION('',(0.,0.,-1.));
#13522=DIRECTION('',(-0.5,-0.866025403784438,0.));
#13523=DIRECTION('center_axis',(0.866025403784439,0.5,0.));
#13524=DIRECTION('ref_axis',(-0.5,0.866025403784439,0.));
#13525=DIRECTION('',(0.5,-0.866025403784439,0.));
#13526=DIRECTION('',(0.,0.,-1.));
#13527=DIRECTION('',(0.5,-0.866025403784439,0.));
#13528=DIRECTION('center_axis',(0.,1.,0.));
#13529=DIRECTION('ref_axis',(0.,0.,1.));
#13530=DIRECTION('',(1.,0.,0.));
#13531=DIRECTION('',(1.,0.,0.));
#13532=DIRECTION('center_axis',(0.,0.,1.));
#13533=DIRECTION('ref_axis',(1.,0.,0.));
#13534=DIRECTION('center_axis',(0.,0.,1.));
#13535=DIRECTION('ref_axis',(1.,0.,0.));
#13536=DIRECTION('center_axis',(0.,0.,1.));
#13537=DIRECTION('ref_axis',(1.,0.,0.));
#16404=CARTESIAN_POINT('',(0.,0.,0.));
#16405=CARTESIAN_POINT('Origin',(0.,0.,16.6));
#16406=CARTESIAN_POINT('',(2.,-2.44929359829471E-16,0.));
#16407=CARTESIAN_POINT('Origin',(0.,0.,0.));
#16408=CARTESIAN_POINT('',(2.,-2.44929359829471E-16,16.6));
#16409=CARTESIAN_POINT('',(2.,-2.44929359829471E-16,16.6));
#16410=CARTESIAN_POINT('Origin',(0.,0.,16.6));
#16411=CARTESIAN_POINT('Origin',(2.3094010767585,-4.,0.));
#16412=CARTESIAN_POINT('',(2.3094010767585,-4.,-4.));
#16413=CARTESIAN_POINT('',(4.61880215351701,0.,-4.));
#16414=CARTESIAN_POINT('',(2.3094010767585,-4.,-4.));
#16415=CARTESIAN_POINT('',(4.61880215351701,0.,0.));
#16416=CARTESIAN_POINT('',(4.61880215351701,0.,0.));
#16417=CARTESIAN_POINT('',(2.3094010767585,-4.,0.));
#16418=CARTESIAN_POINT('',(2.3094010767585,-4.,0.));
#16419=CARTESIAN_POINT('',(2.3094010767585,-4.,0.));
#16420=CARTESIAN_POINT('Origin',(4.61880215351701,0.,0.));
#16421=CARTESIAN_POINT('',(2.3094010767585,4.,-4.));
#16422=CARTESIAN_POINT('',(4.61880215351701,0.,-4.));
#16423=CARTESIAN_POINT('',(2.3094010767585,4.,0.));
#16424=CARTESIAN_POINT('',(2.3094010767585,4.,0.));
#16425=CARTESIAN_POINT('',(4.61880215351701,0.,0.));
#16426=CARTESIAN_POINT('Origin',(2.3094010767585,4.,0.));
#16427=CARTESIAN_POINT('',(-2.3094010767585,4.,-4.));
#16428=CARTESIAN_POINT('',(2.3094010767585,4.,-4.));
#16429=CARTESIAN_POINT('',(-2.3094010767585,4.,0.));
#16430=CARTESIAN_POINT('',(-2.3094010767585,4.,0.));
#16431=CARTESIAN_POINT('',(2.3094010767585,4.,0.));
#16432=CARTESIAN_POINT('Origin',(-2.3094010767585,4.,0.));
#16433=CARTESIAN_POINT('',(-4.61880215351701,5.65640127319951E-16,-4.));
#16434=CARTESIAN_POINT('',(-2.3094010767585,4.,-4.));
#16435=CARTESIAN_POINT('',(-4.61880215351701,5.65640127319951E-16,0.));
#16436=CARTESIAN_POINT('',(-4.61880215351701,5.65640127319951E-16,0.));
#16437=CARTESIAN_POINT('',(-2.3094010767585,4.,0.));
#16438=CARTESIAN_POINT('Origin',(-4.61880215351701,5.65640127319951E-16,
0.));
#16439=CARTESIAN_POINT('',(-2.30940107675851,-4.,-4.));
#16440=CARTESIAN_POINT('',(-4.61880215351701,5.65640127319951E-16,-4.));
#16441=CARTESIAN_POINT('',(-2.30940107675851,-4.,0.));
#16442=CARTESIAN_POINT('',(-2.30940107675851,-4.,0.));
#16443=CARTESIAN_POINT('',(-4.61880215351701,5.65640127319951E-16,0.));
#16444=CARTESIAN_POINT('Origin',(-2.30940107675851,-4.,0.));
#16445=CARTESIAN_POINT('',(-2.30940107675851,-4.,-4.));
#16446=CARTESIAN_POINT('',(-2.30940107675851,-4.,0.));
#16447=CARTESIAN_POINT('Origin',(0.,0.,0.));
#16448=CARTESIAN_POINT('Origin',(0.,0.,-4.));
#16449=CARTESIAN_POINT('Origin',(0.,0.,16.6));
#16570=UNCERTAINTY_MEASURE_WITH_UNIT(LENGTH_MEASURE(0.01),#16599,
'DISTANCE_ACCURACY_VALUE',
'Maximum model space distance between geometric entities at asserted c
onnectivities');
#16572=UNCERTAINTY_MEASURE_WITH_UNIT(LENGTH_MEASURE(0.01),#16599,
'DISTANCE_ACCURACY_VALUE',
'Maximum model space distance between geometric entities at asserted c
onnectivities');
#16596=(
GEOMETRIC_REPRESENTATION_CONTEXT(3)
GLOBAL_UNCERTAINTY_ASSIGNED_CONTEXT((#16570))
GLOBAL_UNIT_ASSIGNED_CONTEXT((#16599,#16601,#16602))
REPRESENTATION_CONTEXT('','3D')
);
#16598=(
GEOMETRIC_REPRESENTATION_CONTEXT(3)
GLOBAL_UNCERTAINTY_ASSIGNED_CONTEXT((#16572))
GLOBAL_UNIT_ASSIGNED_CONTEXT((#16599,#16601,#16602))
REPRESENTATION_CONTEXT('','3D')
);
#16599=(
LENGTH_UNIT()
NAMED_UNIT(*)
SI_UNIT(.MILLI.,.METRE.)
);
#16601=(
NAMED_UNIT(*)
PLANE_ANGLE_UNIT()
SI_UNIT($,.RADIAN.)
);
#16602=(
NAMED_UNIT(*)
SI_UNIT($,.STERADIAN.)
SOLID_ANGLE_UNIT()
);
#16626=SHAPE_DEFINITION_REPRESENTATION(#16651,#16720);
#16651=PRODUCT_DEFINITION_SHAPE('',$,#16746);
#16720=SHAPE_REPRESENTATION('',(#10854),#16596);
#16722=PRODUCT_DEFINITION_CONTEXT('part definition',#16799,'design');
#16746=PRODUCT_DEFINITION('F04_M5_Gib_Adjusting_Screw',
'F04_M5_Gib_Adjusting_Screw',#16771,#16722);
#16771=PRODUCT_DEFINITION_FORMATION('',$,#16824);
#16799=APPLICATION_CONTEXT(
'Core Data for Automotive Mechanical Design Process');
#16800=PRODUCT_CONTEXT('part definition',#16799,'mechanical');
#16824=PRODUCT('F04_M5_Gib_Adjusting_Screw',
'F04_M5_Gib_Adjusting_Screw',$,(#16800));
#16832=PRESENTATION_STYLE_ASSIGNMENT((#16841));
#16841=SURFACE_STYLE_USAGE(.BOTH.,#16850);
#16850=SURFACE_SIDE_STYLE('',(#16859));
#16859=SURFACE_STYLE_FILL_AREA(#16868);
#16868=FILL_AREA_STYLE('Sky Blue',(#16877));
#16877=FILL_AREA_STYLE_COLOUR('Sky Blue',#16886);
#16886=COLOUR_RGB('Sky Blue',0.529411764705882,0.807843137254902,0.92156862745098);
ENDSEC;
END-ISO-10303-21;
